ISO-10303-21;
HEADER;
/* Generated by software containing ST-Developer
 * from STEP Tools, Inc. (www.steptools.com) 
 */

FILE_DESCRIPTION(
/* description */ ('Manual piston pump'),
/* implementation_level */ '2;1');

FILE_NAME(
/* name */ 'Inlet return spring.step',
/* time_stamp */ '2026-11-02T16:54:23-08:00',
/* author */ (''),
/* organization */ (''),
/* preprocessor_version */ 'ST-DEVELOPER v20.2',
/* originating_system */ 'Autodesk Translation Framework v15.17.0.0',
/* authorisation */ '');

FILE_SCHEMA (('AUTOMOTIVE_DESIGN { 1 0 10303 214 3 1 1 }'));
ENDSEC;

DATA;
#10=MECHANICAL_DESIGN_GEOMETRIC_PRESENTATION_REPRESENTATION('',(#727),#19043);
#11=B_SPLINE_SURFACE_WITH_KNOTS('',3,3,((#16647,#16648,#16649,#16650,#16651,
#16652,#16653,#16654,#16655,#16656,#16657,#16658,#16659,#16660,#16661,#16662,
#16663,#16664,#16665,#16666,#16667,#16668,#16669,#16670,#16671,#16672,#16673,
#16674,#16675,#16676,#16677,#16678,#16679,#16680,#16681,#16682,#16683,#16684,
#16685,#16686),(#16687,#16688,#16689,#16690,#16691,#16692,#16693,#16694,
#16695,#16696,#16697,#16698,#16699,#16700,#16701,#16702,#16703,#16704,#16705,
#16706,#16707,#16708,#16709,#16710,#16711,#16712,#16713,#16714,#16715,#16716,
#16717,#16718,#16719,#16720,#16721,#16722,#16723,#16724,#16725,#16726),
(#16727,#16728,#16729,#16730,#16731,#16732,#16733,#16734,#16735,#16736,
#16737,#16738,#16739,#16740,#16741,#16742,#16743,#16744,#16745,#16746,#16747,
#16748,#16749,#16750,#16751,#16752,#16753,#16754,#16755,#16756,#16757,#16758,
#16759,#16760,#16761,#16762,#16763,#16764,#16765,#16766),(#16767,#16768,
#16769,#16770,#16771,#16772,#16773,#16774,#16775,#16776,#16777,#16778,#16779,
#16780,#16781,#16782,#16783,#16784,#16785,#16786,#16787,#16788,#16789,#16790,
#16791,#16792,#16793,#16794,#16795,#16796,#16797,#16798,#16799,#16800,#16801,
#16802,#16803,#16804,#16805,#16806),(#16807,#16808,#16809,#16810,#16811,
#16812,#16813,#16814,#16815,#16816,#16817,#16818,#16819,#16820,#16821,#16822,
#16823,#16824,#16825,#16826,#16827,#16828,#16829,#16830,#16831,#16832,#16833,
#16834,#16835,#16836,#16837,#16838,#16839,#16840,#16841,#16842,#16843,#16844,
#16845,#16846),(#16847,#16848,#16849,#16850,#16851,#16852,#16853,#16854,
#16855,#16856,#16857,#16858,#16859,#16860,#16861,#16862,#16863,#16864,#16865,
#16866,#16867,#16868,#16869,#16870,#16871,#16872,#16873,#16874,#16875,#16876,
#16877,#16878,#16879,#16880,#16881,#16882,#16883,#16884,#16885,#16886),
(#16887,#16888,#16889,#16890,#16891,#16892,#16893,#16894,#16895,#16896,
#16897,#16898,#16899,#16900,#16901,#16902,#16903,#16904,#16905,#16906,#16907,
#16908,#16909,#16910,#16911,#16912,#16913,#16914,#16915,#16916,#16917,#16918,
#16919,#16920,#16921,#16922,#16923,#16924,#16925,#16926),(#16927,#16928,
#16929,#16930,#16931,#16932,#16933,#16934,#16935,#16936,#16937,#16938,#16939,
#16940,#16941,#16942,#16943,#16944,#16945,#16946,#16947,#16948,#16949,#16950,
#16951,#16952,#16953,#16954,#16955,#16956,#16957,#16958,#16959,#16960,#16961,
#16962,#16963,#16964,#16965,#16966),(#16967,#16968,#16969,#16970,#16971,
#16972,#16973,#16974,#16975,#16976,#16977,#16978,#16979,#16980,#16981,#16982,
#16983,#16984,#16985,#16986,#16987,#16988,#16989,#16990,#16991,#16992,#16993,
#16994,#16995,#16996,#16997,#16998,#16999,#17000,#17001,#17002,#17003,#17004,
#17005,#17006),(#17007,#17008,#17009,#17010,#17011,#17012,#17013,#17014,
#17015,#17016,#17017,#17018,#17019,#17020,#17021,#17022,#17023,#17024,#17025,
#17026,#17027,#17028,#17029,#17030,#17031,#17032,#17033,#17034,#17035,#17036,
#17037,#17038,#17039,#17040,#17041,#17042,#17043,#17044,#17045,#17046),
(#17047,#17048,#17049,#17050,#17051,#17052,#17053,#17054,#17055,#17056,
#17057,#17058,#17059,#17060,#17061,#17062,#17063,#17064,#17065,#17066,#17067,
#17068,#17069,#17070,#17071,#17072,#17073,#17074,#17075,#17076,#17077,#17078,
#17079,#17080,#17081,#17082,#17083,#17084,#17085,#17086),(#17087,#17088,
#17089,#17090,#17091,#17092,#17093,#17094,#17095,#17096,#17097,#17098,#17099,
#17100,#17101,#17102,#17103,#17104,#17105,#17106,#17107,#17108,#17109,#17110,
#17111,#17112,#17113,#17114,#17115,#17116,#17117,#17118,#17119,#17120,#17121,
#17122,#17123,#17124,#17125,#17126)),.UNSPECIFIED.,.T.,.F.,.F.,(4,1,1,1,
1,1,1,1,1,4),(4,1,1,1,1,1,1,1,1,1,1,1,1,1,1,1,1,1,1,1,1,1,1,1,1,1,1,1,1,
1,1,1,1,1,1,1,1,4),(-3.14159265358979,-2.46839422782055,-2.24399475256414,
-1.79519580205131,-1.12199737628207,-0.448798950512828,0.448798950512828,
1.34639685153848,2.24399475256414,3.14159265358979),(0.,0.0178571428571429,
0.0357142857142857,0.0714285714285714,0.107142857142857,0.142857142857143,
0.154761904761905,0.166666666666667,0.19047619047619,0.214285714285714,
0.232142857142857,0.25,0.267857142857143,0.285714285714286,0.303571428571429,
0.321428571428571,0.357142857142857,0.375,0.392857142857143,0.428571428571429,
0.464285714285714,0.5,0.535714285714286,0.571428571428571,0.607142857142857,
0.642857142857143,0.678571428571428,0.714285714285714,0.75,0.785714285714286,
0.821428571428571,0.857142857142857,0.892857142857143,0.928571428571429,
0.946428571428571,0.964285714285714,0.982142857142857,1.),.UNSPECIFIED.);
#593=SHAPE_REPRESENTATION_RELATIONSHIP('SRR','None',#19340,#656);
#656=ADVANCED_BREP_SHAPE_REPRESENTATION('',(#797),#19007);
#727=STYLED_ITEM('',(#19664),#797);
#797=MANIFOLD_SOLID_BREP('Body1',#9513);
#1073=B_SPLINE_CURVE_WITH_KNOTS('',3,(#17130,#17131,#17132,#17133,#17134,
#17135,#17136,#17137,#17138,#17139,#17140,#17141,#17142,#17143,#17144,#17145,
#17146,#17147,#17148,#17149,#17150,#17151,#17152,#17153,#17154,#17155,#17156,
#17157,#17158,#17159,#17160,#17161,#17162,#17163,#17164,#17165,#17166,#17167,
#17168,#17169),.UNSPECIFIED.,.F.,.F.,(4,1,1,1,1,1,1,1,1,1,1,1,1,1,1,1,1,
1,1,1,1,1,1,1,1,1,1,1,1,1,1,1,1,1,1,1,1,4),(0.,0.0178571428571429,0.0357142857142857,
0.0714285714285714,0.107142857142857,0.142857142857143,0.154761904761905,
0.166666666666667,0.19047619047619,0.214285714285714,0.232142857142857,
0.25,0.267857142857143,0.285714285714286,0.303571428571429,0.321428571428571,
0.357142857142857,0.375,0.392857142857143,0.428571428571429,0.464285714285714,
0.5,0.535714285714286,0.571428571428571,0.607142857142857,0.642857142857143,
0.678571428571428,0.714285714285714,0.75,0.785714285714286,0.821428571428571,
0.857142857142857,0.892857142857143,0.928571428571429,0.946428571428571,
0.964285714285714,0.982142857142857,1.),.UNSPECIFIED.);
#1634=FACE_OUTER_BOUND('',#2366,.T.);
#1635=FACE_OUTER_BOUND('',#2367,.T.);
#1636=FACE_OUTER_BOUND('',#2368,.T.);
#2366=EDGE_LOOP('',(#7701,#7702,#7703,#7704));
#2367=EDGE_LOOP('',(#7705));
#2368=EDGE_LOOP('',(#7706));
#2986=CIRCLE('',#10955,0.025);
#2987=CIRCLE('',#10956,0.025);
#4836=VERTEX_POINT('',#17127);
#4837=VERTEX_POINT('',#17129);
#5837=EDGE_CURVE('',#4836,#4836,#2986,.T.);
#5838=EDGE_CURVE('',#4836,#4837,#1073,.T.);
#5839=EDGE_CURVE('',#4837,#4837,#2987,.T.);
#7701=ORIENTED_EDGE('',*,*,#5837,.T.);
#7702=ORIENTED_EDGE('',*,*,#5838,.T.);
#7703=ORIENTED_EDGE('',*,*,#5839,.F.);
#7704=ORIENTED_EDGE('',*,*,#5838,.F.);
#7705=ORIENTED_EDGE('',*,*,#5839,.T.);
#7706=ORIENTED_EDGE('',*,*,#5837,.F.);
#8750=PLANE('',#10957);
#8751=PLANE('',#10958);
#9239=ADVANCED_FACE('',(#1634),#11,.T.);
#9240=ADVANCED_FACE('',(#1635),#8750,.T.);
#9241=ADVANCED_FACE('',(#1636),#8751,.F.);
#9513=CLOSED_SHELL('',(#9239,#9240,#9241));
#10954=AXIS2_PLACEMENT_3D('',#16646,#13264,#13265);
#10955=AXIS2_PLACEMENT_3D('',#17128,#13266,#13267);
#10956=AXIS2_PLACEMENT_3D('',#17170,#13268,#13269);
#10957=AXIS2_PLACEMENT_3D('',#17171,#13270,#13271);
#10958=AXIS2_PLACEMENT_3D('',#17172,#13272,#13273);
#13264=DIRECTION('axis',(0.,0.,1.));
#13265=DIRECTION('refdir',(1.,0.,0.));
#13266=DIRECTION('center_axis',(-0.000136055539638692,0.998234251987705,
0.0593999970322941));
#13267=DIRECTION('ref_axis',(8.09599406112E-6,-0.0593999964805675,0.998234261259632));
#13268=DIRECTION('center_axis',(0.000136055901346167,0.998234251958982,
0.0593999975141763));
#13269=DIRECTION('ref_axis',(-0.901400654247254,-0.0255969411270683,0.432228709281972));
#13270=DIRECTION('center_axis',(0.000136055901346167,0.998234251958982,
0.0593999975141763));
#13271=DIRECTION('ref_axis',(-0.901400654247254,-0.0255969411270683,0.432228709281972));
#13272=DIRECTION('center_axis',(-0.000136055539638692,0.998234251987705,
0.0593999970322941));
#13273=DIRECTION('ref_axis',(8.09599406112E-6,-0.0593999964805675,0.998234261259632));
#16646=CARTESIAN_POINT('',(0.,0.,0.));
#16647=CARTESIAN_POINT('Ctrl Pts',(-1.30000020239985,11.401484999912,8.08504414346851));
#16648=CARTESIAN_POINT('Ctrl Pts',(-1.30000327196951,11.4240063142585,8.08638427580987));
#16649=CARTESIAN_POINT('Ctrl Pts',(-1.30766195210704,11.4688296121143,8.08906540106247));
#16650=CARTESIAN_POINT('Ctrl Pts',(-1.35170527056063,11.5490007767019,8.09444309083296));
#16651=CARTESIAN_POINT('Ctrl Pts',(-1.45277519214087,11.6127580060184,8.10118931860474));
#16652=CARTESIAN_POINT('Ctrl Pts',(-1.59631200820559,11.5967080298454,8.10932541726778));
#16653=CARTESIAN_POINT('Ctrl Pts',(-1.67596957869062,11.5170338262931,8.11568426491253));
#16654=CARTESIAN_POINT('Ctrl Pts',(-1.70121188840275,11.4444384060934,8.1202410535319));
#16655=CARTESIAN_POINT('Ctrl Pts',(-1.70818405294183,11.3832823318955,8.12389232718534));
#16656=CARTESIAN_POINT('Ctrl Pts',(-1.69072329377588,11.3066287277546,8.12846738314285));
#16657=CARTESIAN_POINT('Ctrl Pts',(-1.63665950516375,11.238790127298,8.13351592412261));
#16658=CARTESIAN_POINT('Ctrl Pts',(-1.56818361973235,11.2009745480362,8.13811814384478));
#16659=CARTESIAN_POINT('Ctrl Pts',(-1.49863040169783,11.1891308835848,8.14226983820643));
#16660=CARTESIAN_POINT('Ctrl Pts',(-1.42891504240342,11.200968879272,8.14643117635655));
#16661=CARTESIAN_POINT('Ctrl Pts',(-1.3668378439393,11.2352429623094,8.1506021000395));
#16662=CARTESIAN_POINT('Ctrl Pts',(-1.31955925093111,11.28820773555,8.15478254820105));
#16663=CARTESIAN_POINT('Ctrl Pts',(-1.2829867844608,11.3759192191191,8.16036908991613));
#16664=CARTESIAN_POINT('Ctrl Pts',(-1.29401152106405,11.4745465130164,8.16597441543018));
#16665=CARTESIAN_POINT('Ctrl Pts',(-1.34954004839579,11.552412334257,8.17159821912675));
#16666=CARTESIAN_POINT('Ctrl Pts',(-1.42751096236488,11.6080171412814,8.17723423461392));
#16667=CARTESIAN_POINT('Ctrl Pts',(-1.55195451138358,11.6222672514631,8.18430195037065));
#16668=CARTESIAN_POINT('Ctrl Pts',(-1.68004289685552,11.5419454250746,8.19281879836256));
#16669=CARTESIAN_POINT('Ctrl Pts',(-1.73003116645036,11.3988109655711,8.20137045479898));
#16670=CARTESIAN_POINT('Ctrl Pts',(-1.67986342570098,11.2550353636857,8.20995610504997));
#16671=CARTESIAN_POINT('Ctrl Pts',(-1.55045492335515,11.1736299517761,8.21857485832766));
#16672=CARTESIAN_POINT('Ctrl Pts',(-1.39801143573852,11.1907087568511,8.22722577082007));
#16673=CARTESIAN_POINT('Ctrl Pts',(-1.28896559860806,11.2995363829214,8.23590787035433));
#16674=CARTESIAN_POINT('Ctrl Pts',(-1.27176576818906,11.4530596594369,8.2446200855233));
#16675=CARTESIAN_POINT('Ctrl Pts',(-1.35415676648766,11.5843816465237,8.25336136935291));
#16676=CARTESIAN_POINT('Ctrl Pts',(-1.50092826267245,11.6358042592741,8.26213056504353));
#16677=CARTESIAN_POINT('Ctrl Pts',(-1.64822931811663,11.5845480275544,8.27092648209213));
#16678=CARTESIAN_POINT('Ctrl Pts',(-1.73150905278482,11.452001965896,8.27974794260049));
#16679=CARTESIAN_POINT('Ctrl Pts',(-1.71403680175737,11.2961559302974,8.28859365842336));
#16680=CARTESIAN_POINT('Ctrl Pts',(-1.60280104690191,11.1847900297702,8.2974622924596));
#16681=CARTESIAN_POINT('Ctrl Pts',(-1.47233026209572,11.1701693264817,8.30487091671699));
#16682=CARTESIAN_POINT('Ctrl Pts',(-1.37913177644534,11.2089883543221,8.31080779458597));
#16683=CARTESIAN_POINT('Ctrl Pts',(-1.32263542974685,11.2593763422036,8.31526551319425));
#16684=CARTESIAN_POINT('Ctrl Pts',(-1.28594863227905,11.3258070419811,8.31972744443214));
#16685=CARTESIAN_POINT('Ctrl Pts',(-1.27746839178067,11.3756346212766,8.3227063400453));
#16686=CARTESIAN_POINT('Ctrl Pts',(-1.27746498364382,11.4006399235282,8.32419428226795));
#16687=CARTESIAN_POINT('Ctrl Pts',(-1.30561018922915,11.4014842352921,8.08504414346851));
#16688=CARTESIAN_POINT('Ctrl Pts',(-1.30561317376826,11.4233816837205,8.086347152626));
#16689=CARTESIAN_POINT('Ctrl Pts',(-1.31305775063703,11.4669500532733,8.08895315356629));
#16690=CARTESIAN_POINT('Ctrl Pts',(-1.35587389923117,11.5448896113668,8.09418109446772));
#16691=CARTESIAN_POINT('Ctrl Pts',(-1.45414237109159,11.6068834959059,8.1007401673878));
#16692=CARTESIAN_POINT('Ctrl Pts',(-1.59373635323225,11.5912809574038,8.10865257057474));
#16693=CARTESIAN_POINT('Ctrl Pts',(-1.67123187587081,11.5137779191814,8.11483818917685));
#16694=CARTESIAN_POINT('Ctrl Pts',(-1.69579348728882,11.4431421204579,8.11927193653773));
#16695=CARTESIAN_POINT('Ctrl Pts',(-1.70257863279989,11.3836303806017,8.12282501375471));
#16696=CARTESIAN_POINT('Ctrl Pts',(-1.68558654139025,11.3090241994265,8.12727779004479));
#16697=CARTESIAN_POINT('Ctrl Pts',(-1.63295615848599,11.2429798931532,8.13219258288139));
#16698=CARTESIAN_POINT('Ctrl Pts',(-1.566278348169,11.2061554948114,8.13667389502812));
#16699=CARTESIAN_POINT('Ctrl Pts',(-1.49853679575807,11.1946189405735,8.14071738115773));
#16700=CARTESIAN_POINT('Ctrl Pts',(-1.43062202860689,11.2061497948702,8.14477112824115));
#16701=CARTESIAN_POINT('Ctrl Pts',(-1.37013382675731,11.2395448898541,8.14883515208722));
#16702=CARTESIAN_POINT('Ctrl Pts',(-1.32405401153072,11.2911647817536,8.15290938776615));
#16703=CARTESIAN_POINT('Ctrl Pts',(-1.2883990061143,11.3766703427473,8.15835541715125));
#16704=CARTESIAN_POINT('Ctrl Pts',(-1.29914297476456,11.4728556938531,8.16382140249562));
#16705=CARTESIAN_POINT('Ctrl Pts',(-1.35331704713924,11.5488262135619,8.16930807813071));
#16706=CARTESIAN_POINT('Ctrl Pts',(-1.42940812666591,11.603093047596,8.17480820693407));
#16707=CARTESIAN_POINT('Ctrl Pts',(-1.5509044986295,11.6170176339805,8.18170806918465));
#16708=CARTESIAN_POINT('Ctrl Pts',(-1.67604613105416,11.5385632076231,8.1900276948735));
#16709=CARTESIAN_POINT('Ctrl Pts',(-1.72492790563121,11.3986468322849,8.19838704499274));
#16710=CARTESIAN_POINT('Ctrl Pts',(-1.67587099510752,11.2579997087285,8.20678486638522));
#16711=CARTESIAN_POINT('Ctrl Pts',(-1.54920582156964,11.1782977772372,8.21522087138253));
#16712=CARTESIAN_POINT('Ctrl Pts',(-1.39987270237286,11.1950092739017,8.22369456459123));
#16713=CARTESIAN_POINT('Ctrl Pts',(-1.29296012904138,11.3016805955749,8.23220484911079));
#16714=CARTESIAN_POINT('Ctrl Pts',(-1.27606634663982,11.4522974351608,8.24075185134853));
#16715=CARTESIAN_POINT('Ctrl Pts',(-1.35694591802673,11.581247543156,8.24933365411482));
#16716=CARTESIAN_POINT('Ctrl Pts',(-1.5011662508949,11.6317982852345,8.2579498683441));
#16717=CARTESIAN_POINT('Ctrl Pts',(-1.64604163901749,11.5814097661045,8.2666000286487));
#16718=CARTESIAN_POINT('Ctrl Pts',(-1.72803741960536,11.4509543091606,8.27528200509536));
#16719=CARTESIAN_POINT('Ctrl Pts',(-1.71084979806451,11.2974158009061,8.28399568222005));
#16720=CARTESIAN_POINT('Ctrl Pts',(-1.60118525501138,11.1875858779187,8.29273967518402));
#16721=CARTESIAN_POINT('Ctrl Pts',(-1.47242352789517,11.1731365127125,8.30005053314264));
#16722=CARTESIAN_POINT('Ctrl Pts',(-1.38037678027956,11.2114713043444,8.30591365435341));
#16723=CARTESIAN_POINT('Ctrl Pts',(-1.32455318945295,11.2612572045339,8.31031798968997));
#16724=CARTESIAN_POINT('Ctrl Pts',(-1.28828503889033,11.3269239200058,8.31472851044227));
#16725=CARTESIAN_POINT('Ctrl Pts',(-1.2798974005807,11.3762050216631,8.31767449100403));
#16726=CARTESIAN_POINT('Ctrl Pts',(-1.2798940292022,11.4009406300668,8.3191463850758));
#16727=CARTESIAN_POINT('Ctrl Pts',(-1.31306297036576,11.4013274969404,8.08766110654672));
#16728=CARTESIAN_POINT('Ctrl Pts',(-1.31306584176654,11.4223948538255,8.08891472105049));
#16729=CARTESIAN_POINT('Ctrl Pts',(-1.32022595841211,11.4642913196188,8.09142088120675));
#16730=CARTESIAN_POINT('Ctrl Pts',(-1.3613966361963,11.5392328901146,8.0964478876486));
#16731=CARTESIAN_POINT('Ctrl Pts',(-1.45586891668678,11.5988239699255,8.10275392212449));
#16732=CARTESIAN_POINT('Ctrl Pts',(-1.59003358409734,11.5838224866908,8.11035899573519));
#16733=CARTESIAN_POINT('Ctrl Pts',(-1.66450268829473,11.5093423753564,8.1163037475407));
#16734=CARTESIAN_POINT('Ctrl Pts',(-1.68810388128966,11.4414683120752,8.12056421907664));
#16735=CARTESIAN_POINT('Ctrl Pts',(-1.69462346644093,11.3842846793712,8.12397836072229));
#16736=CARTESIAN_POINT('Ctrl Pts',(-1.67829634268994,11.3125987667127,8.12825695359797));
#16737=CARTESIAN_POINT('Ctrl Pts',(-1.62772606180868,11.2491396082833,8.13297955674803));
#16738=CARTESIAN_POINT('Ctrl Pts',(-1.56365666335395,11.2137555492106,8.13728579433529));
#16739=CARTESIAN_POINT('Ctrl Pts',(-1.49856276330161,11.2026696594146,8.14117141515599));
#16740=CARTESIAN_POINT('Ctrl Pts',(-1.43329887044197,11.2137500860466,8.1450671353107));
#16741=CARTESIAN_POINT('Ctrl Pts',(-1.37516753872871,11.2458433998655,8.14897297344427));
#16742=CARTESIAN_POINT('Ctrl Pts',(-1.33087918806968,11.2954557031031,8.15288901470097));
#16743=CARTESIAN_POINT('Ctrl Pts',(-1.29660656832626,11.3776436947897,8.15812395380951));
#16744=CARTESIAN_POINT('Ctrl Pts',(-1.30693144068213,11.4701150917588,8.16337975545564));
#16745=CARTESIAN_POINT('Ctrl Pts',(-1.35902331625725,11.543168042114,8.1686558456901));
#16746=CARTESIAN_POINT('Ctrl Pts',(-1.4322019409561,11.5953592388398,8.17394571966293));
#16747=CARTESIAN_POINT('Ctrl Pts',(-1.54907958898726,11.6087617453262,8.18058425953556));
#16748=CARTESIAN_POINT('Ctrl Pts',(-1.66951924414406,11.5332671141026,8.18859204271931));
#16749=CARTESIAN_POINT('Ctrl Pts',(-1.71659538358893,11.3985548288704,8.19664119986952));
#16750=CARTESIAN_POINT('Ctrl Pts',(-1.66934869204329,11.263060224324,8.20473213005192));
#16751=CARTESIAN_POINT('Ctrl Pts',(-1.54726459234342,11.1862242141209,8.21286457991536));
#16752=CARTESIAN_POINT('Ctrl Pts',(-1.403231716151,11.2023264846078,8.22103831570913));
#16753=CARTESIAN_POINT('Ctrl Pts',(-1.30003232284203,11.3052671100812,8.22925331150977));
#16754=CARTESIAN_POINT('Ctrl Pts',(-1.28369656143046,11.4507366860132,8.23750884780489));
#16755=CARTESIAN_POINT('Ctrl Pts',(-1.36185526146802,11.5753880610041,8.24580509426953));
#16756=CARTESIAN_POINT('Ctrl Pts',(-1.50136129039097,11.6243092053923,8.25414140440729));
#16757=CARTESIAN_POINT('Ctrl Pts',(-1.64163448696699,11.575543781206,8.26251708791278));
#16758=CARTESIAN_POINT('Ctrl Pts',(-1.72111161664867,11.4491347895288,8.27093210201896));
#16759=CARTESIAN_POINT('Ctrl Pts',(-1.7044604276663,11.3002021021866,8.2793854617994));
#16760=CARTESIAN_POINT('Ctrl Pts',(-1.59799858575781,11.1935458453921,8.28787653903472));
#16761=CARTESIAN_POINT('Ctrl Pts',(-1.47284948855244,11.1794809358239,8.29498349615704));
#16762=CARTESIAN_POINT('Ctrl Pts',(-1.38331353640591,11.2167639858896,8.30068679568983));
#16763=CARTESIAN_POINT('Ctrl Pts',(-1.32898237958042,11.265213989999,8.30497353649788));
#16764=CARTESIAN_POINT('Ctrl Pts',(-1.29366313251612,11.3291522904247,8.30926836315146));
#16765=CARTESIAN_POINT('Ctrl Pts',(-1.28548737860853,11.377165793908,8.31213893807902));
#16766=CARTESIAN_POINT('Ctrl Pts',(-1.28548409287768,11.4012730104724,8.31357343965136));
#16767=CARTESIAN_POINT('Ctrl Pts',(-1.32103424175969,11.4008514651028,8.09564270205866));
#16768=CARTESIAN_POINT('Ctrl Pts',(-1.32103699195541,11.4210295451449,8.09684340008343));
#16769=CARTESIAN_POINT('Ctrl Pts',(-1.32789231710736,11.4611316789685,8.0992420730212));
#16770=CARTESIAN_POINT('Ctrl Pts',(-1.36727547823986,11.5328077470696,8.10405001399985));
#16771=CARTESIAN_POINT('Ctrl Pts',(-1.45754711739153,11.5897214854973,8.11007410615735));
#16772=CARTESIAN_POINT('Ctrl Pts',(-1.58554555854653,11.5753779241661,8.11732936867022));
#16773=CARTESIAN_POINT('Ctrl Pts',(-1.65648647122026,11.5043959899759,8.12299301563456));
#16774=CARTESIAN_POINT('Ctrl Pts',(-1.67895482165105,11.4397741970643,8.12704923413514));
#16775=CARTESIAN_POINT('Ctrl Pts',(-1.68515842268585,11.3853512093574,8.13029844296023));
#16776=CARTESIAN_POINT('Ctrl Pts',(-1.66962265478899,11.317166679158,8.13436799177394));
#16777=CARTESIAN_POINT('Ctrl Pts',(-1.62155125823249,11.2568528248445,8.13885658269807));
#16778=CARTESIAN_POINT('Ctrl Pts',(-1.5606882470131,11.2232428458746,8.14294697076423));
#16779=CARTESIAN_POINT('Ctrl Pts',(-1.49888250925831,11.2127193333593,8.14663610445338));
#16780=CARTESIAN_POINT('Ctrl Pts',(-1.43694440041945,11.2232373643193,8.15033311420883));
#16781=CARTESIAN_POINT('Ctrl Pts',(-1.38179993687197,11.2536842303237,8.15403815979746));
#16782=CARTESIAN_POINT('Ctrl Pts',(-1.33980484758458,11.3007302610076,8.15775132662947));
#16783=CARTESIAN_POINT('Ctrl Pts',(-1.30732081947074,11.3786370745734,8.16271331530134));
#16784=CARTESIAN_POINT('Ctrl Pts',(-1.31711167307388,11.4662407990072,8.16769172469551));
#16785=CARTESIAN_POINT('Ctrl Pts',(-1.36644128702568,11.535416047879,8.17268772160113));
#16786=CARTESIAN_POINT('Ctrl Pts',(-1.43571925164195,11.5848227687984,8.17769535472986));
#16787=CARTESIAN_POINT('Ctrl Pts',(-1.54632194219297,11.5974965778118,8.18397667082501));
#16788=CARTESIAN_POINT('Ctrl Pts',(-1.66024126283624,11.526078645737,8.19155040003289));
#16789=CARTESIAN_POINT('Ctrl Pts',(-1.70475017825474,11.398693466046,8.19916124463926));
#16790=CARTESIAN_POINT('Ctrl Pts',(-1.66008089559322,11.2706019001248,8.20680943547037));
#16791=CARTESIAN_POINT('Ctrl Pts',(-1.54468129549965,11.1979748206298,8.21449577476897));
#16792=CARTESIAN_POINT('Ctrl Pts',(-1.40854209175388,11.2131945094957,8.22222091002894));
#16793=CARTESIAN_POINT('Ctrl Pts',(-1.31099292984935,11.3104962046553,8.22998512334889));
#16794=CARTESIAN_POINT('Ctrl Pts',(-1.29554561676741,11.4480189253003,8.23778933163032));
#16795=CARTESIAN_POINT('Ctrl Pts',(-1.36944655967922,11.565890347967,8.24563332598042));
#16796=CARTESIAN_POINT('Ctrl Pts',(-1.50140057214675,11.6121713702853,8.25351766479738));
#16797=CARTESIAN_POINT('Ctrl Pts',(-1.63413904066431,11.5660364884835,8.26144283720535));
#16798=CARTESIAN_POINT('Ctrl Pts',(-1.70939315545077,11.4463700948655,8.26940843154104));
#16799=CARTESIAN_POINT('Ctrl Pts',(-1.69363648017702,11.3052927092352,8.27741504805892));
#16800=CARTESIAN_POINT('Ctrl Pts',(-1.59274015694463,11.2041861132693,8.2854625305572));
#16801=CARTESIAN_POINT('Ctrl Pts',(-1.47403588655886,11.1908297218178,8.29220284433934));
#16802=CARTESIAN_POINT('Ctrl Pts',(-1.38905600055158,11.2262117116569,8.29761560138678));
#16803=CARTESIAN_POINT('Ctrl Pts',(-1.33746800584448,11.2722131459904,8.3016856127907));
#16804=CARTESIAN_POINT('Ctrl Pts',(-1.30391657347503,11.3329466374338,8.30576509541387));
#16805=CARTESIAN_POINT('Ctrl Pts',(-1.29614603551713,11.3785729716546,8.30849275036084));
#16806=CARTESIAN_POINT('Ctrl Pts',(-1.29614291123828,11.4014956242496,8.30985676437308));
#16807=CARTESIAN_POINT('Ctrl Pts',(-1.3260670098578,11.4002349190591,8.10599241036715));
#16808=CARTESIAN_POINT('Ctrl Pts',(-1.32606968291948,11.4198470696096,8.10715943271904));
#16809=CARTESIAN_POINT('Ctrl Pts',(-1.33273281226418,11.4588038723593,8.10948976421575));
#16810=CARTESIAN_POINT('Ctrl Pts',(-1.37095440763743,11.5283461686134,8.11415485784104));
#16811=CARTESIAN_POINT('Ctrl Pts',(-1.45842218727122,11.5834480956078,8.1199908943121));
#16812=CARTESIAN_POINT('Ctrl Pts',(-1.58214016743539,11.5695361488843,8.12700402166414));
#16813=CARTESIAN_POINT('Ctrl Pts',(-1.6505461986618,11.5010454928845,8.1324675549927));
#16814=CARTESIAN_POINT('Ctrl Pts',(-1.67218692028815,11.438796213927,8.13637491600817));
#16815=CARTESIAN_POINT('Ctrl Pts',(-1.67815707268655,11.3864050605593,8.13950281778127));
#16816=CARTESIAN_POINT('Ctrl Pts',(-1.66320671049994,11.3208332987116,8.14341662245883));
#16817=CARTESIAN_POINT('Ctrl Pts',(-1.6170263802457,11.2629087351497,8.14772800364013));
#16818=CARTESIAN_POINT('Ctrl Pts',(-1.55862855664036,11.2306659472504,8.15165270938754));
#16819=CARTESIAN_POINT('Ctrl Pts',(-1.49938112584704,11.2205825413491,8.15518919749908));
#16820=CARTESIAN_POINT('Ctrl Pts',(-1.44006051390674,11.230660480028,8.15873013742039));
#16821=CARTESIAN_POINT('Ctrl Pts',(-1.38729324228833,11.2597999378773,8.16227571569575));
#16822=CARTESIAN_POINT('Ctrl Pts',(-1.34714332103464,11.3047845473531,8.16582612996534));
#16823=CARTESIAN_POINT('Ctrl Pts',(-1.31611489452621,11.3792166484954,8.17056669239132));
#16824=CARTESIAN_POINT('Ctrl Pts',(-1.32547786817095,11.4628087458619,8.17531773240094));
#16825=CARTESIAN_POINT('Ctrl Pts',(-1.37250076638947,11.5287400964063,8.18007984615502));
#16826=CARTESIAN_POINT('Ctrl Pts',(-1.43849039681914,11.5757957350937,8.18484962468035));
#16827=CARTESIAN_POINT('Ctrl Pts',(-1.5437319225136,11.5878314837568,8.19082671867637));
#16828=CARTESIAN_POINT('Ctrl Pts',(-1.65197121086361,11.5199414851004,8.19802432278872));
#16829=CARTESIAN_POINT('Ctrl Pts',(-1.6941932541106,11.3990279346596,8.2052483285463));
#16830=CARTESIAN_POINT('Ctrl Pts',(-1.65182013218686,11.2775902099755,8.21250011259887));
#16831=CARTESIAN_POINT('Ctrl Pts',(-1.5425053138839,11.208816960598,8.21978090905886));
#16832=CARTESIAN_POINT('Ctrl Pts',(-1.41367307841592,11.2232379205072,8.22709192200815));
#16833=CARTESIAN_POINT('Ctrl Pts',(-1.32144158430647,11.3152580680232,8.23443434009105));
#16834=CARTESIAN_POINT('Ctrl Pts',(-1.30685791506974,11.4452123640102,8.24180922112913));
#16835=CARTESIAN_POINT('Ctrl Pts',(-1.37666067193666,11.5565256246853,8.24921769750194));
#16836=CARTESIAN_POINT('Ctrl Pts',(-1.50122376802224,11.6002043298051,8.25666074862816));
#16837=CARTESIAN_POINT('Ctrl Pts',(-1.62647535881528,11.5566634330241,8.26413930384511));
#16838=CARTESIAN_POINT('Ctrl Pts',(-1.69746195702876,11.4437715041625,8.27165430693189));
#16839=CARTESIAN_POINT('Ctrl Pts',(-1.68259639325137,11.3107071182644,8.27920658135681));
#16840=CARTESIAN_POINT('Ctrl Pts',(-1.58743666439843,11.2153502096692,8.28679684916848));
#16841=CARTESIAN_POINT('Ctrl Pts',(-1.47547877159778,11.2027509304328,8.29315446469811));
#16842=CARTESIAN_POINT('Ctrl Pts',(-1.39532198921553,11.2361236546606,8.2982601024122));
#16843=CARTESIAN_POINT('Ctrl Pts',(-1.34665715381,11.2795168939374,8.30209953408665));
#16844=CARTESIAN_POINT('Ctrl Pts',(-1.31500353192678,11.3368140047837,8.30594831599043));
#16845=CARTESIAN_POINT('Ctrl Pts',(-1.30767075102972,11.3798594828672,8.30852180942975));
#16846=CARTESIAN_POINT('Ctrl Pts',(-1.30766780150076,11.4015000057239,8.30980953022411));
#16847=CARTESIAN_POINT('Ctrl Pts',(-1.32429511903454,11.3993031065134,8.12165585012413));
#16848=CARTESIAN_POINT('Ctrl Pts',(-1.32429781781632,11.4191039644791,8.1228341015236));
#16849=CARTESIAN_POINT('Ctrl Pts',(-1.33102804386872,11.4584301358476,8.12518651179406));
#16850=CARTESIAN_POINT('Ctrl Pts',(-1.3695473849912,11.5284828501307,8.12988606294773));
#16851=CARTESIAN_POINT('Ctrl Pts',(-1.4574640817777,11.5837998736453,8.13574965708596));
#16852=CARTESIAN_POINT('Ctrl Pts',(-1.58131263137073,11.569792551805,8.14277036400045));
#16853=CARTESIAN_POINT('Ctrl Pts',(-1.64950649882507,11.5014332536728,8.14822001424199));
#16854=CARTESIAN_POINT('Ctrl Pts',(-1.67103635899034,11.4394876061675,8.15210827606713));
#16855=CARTESIAN_POINT('Ctrl Pts',(-1.6769669951888,11.3874129860507,8.15521716270536));
#16856=CARTESIAN_POINT('Ctrl Pts',(-1.66211632286131,11.3223602958148,8.15910015158052));
#16857=CARTESIAN_POINT('Ctrl Pts',(-1.61639293949884,11.2650405356275,8.16336732839958));
#16858=CARTESIAN_POINT('Ctrl Pts',(-1.55870840547367,11.2332032111892,8.16724366666583));
#16859=CARTESIAN_POINT('Ctrl Pts',(-1.50029173796469,11.2232701523227,8.17073037999097));
#16860=CARTESIAN_POINT('Ctrl Pts',(-1.44190956391688,11.2331975359923,8.17421528166781));
#16861=CARTESIAN_POINT('Ctrl Pts',(-1.3900717844478,11.2618342173886,8.17769861066017));
#16862=CARTESIAN_POINT('Ctrl Pts',(-1.35070110243207,11.3059575230339,8.18118055114061));
#16863=CARTESIAN_POINT('Ctrl Pts',(-1.3203344326381,11.3788365850552,8.18582165533132));
#16864=CARTESIAN_POINT('Ctrl Pts',(-1.32952184495293,11.4604584388187,8.19046061601537));
#16865=CARTESIAN_POINT('Ctrl Pts',(-1.37533045200066,11.5246661042799,8.19509882898403));
#16866=CARTESIAN_POINT('Ctrl Pts',(-1.43950399975653,11.5704131054485,8.19973665995863));
#16867=CARTESIAN_POINT('Ctrl Pts',(-1.54158688211486,11.5820306841873,8.20553354749156));
#16868=CARTESIAN_POINT('Ctrl Pts',(-1.64618759928906,11.5163399534721,8.21249128355902));
#16869=CARTESIAN_POINT('Ctrl Pts',(-1.68681134598222,11.3998046741489,8.21945237306914));
#16870=CARTESIAN_POINT('Ctrl Pts',(-1.64604585564518,11.2831703620476,8.22641822854091));
#16871=CARTESIAN_POINT('Ctrl Pts',(-1.54132195608804,11.2173597607551,8.23339069515916));
#16872=CARTESIAN_POINT('Ctrl Pts',(-1.41830938390692,11.2311901718608,8.2403715442691));
#16873=CARTESIAN_POINT('Ctrl Pts',(-1.33053222526684,11.3188506935694,8.24736231765686));
#16874=CARTESIAN_POINT('Ctrl Pts',(-1.31674033947129,11.4422539514988,8.25436502694203));
#16875=CARTESIAN_POINT('Ctrl Pts',(-1.38289384830905,11.5476448074141,8.2613809340997));
#16876=CARTESIAN_POINT('Ctrl Pts',(-1.50058265035914,11.5888574428762,8.26841185165828));
#16877=CARTESIAN_POINT('Ctrl Pts',(-1.61860649329354,11.5477766859291,8.27545955861919));
#16878=CARTESIAN_POINT('Ctrl Pts',(-1.6853122808406,11.4416028775854,8.2825252382829));
#16879=CARTESIAN_POINT('Ctrl Pts',(-1.67132138430609,11.3167601085876,8.28961078326854));
#16880=CARTESIAN_POINT('Ctrl Pts',(-1.58218915935843,11.2275025938439,8.29671759533642));
#16881=CARTESIAN_POINT('Ctrl Pts',(-1.47755351447608,11.215757788223,8.30265888951343));
#16882=CARTESIAN_POINT('Ctrl Pts',(-1.40274312459196,11.2469117151256,8.30742416231202));
#16883=CARTESIAN_POINT('Ctrl Pts',(-1.35736260532778,11.2873801550968,8.31100447713038));
#16884=CARTESIAN_POINT('Ctrl Pts',(-1.32787172938268,11.3407752864055,8.3145909371932));
#16885=CARTESIAN_POINT('Ctrl Pts',(-1.32104740977581,11.3808439865734,8.31698635026477));
#16886=CARTESIAN_POINT('Ctrl Pts',(-1.3210446621183,11.4010033902875,8.31818593696314));
#16887=CARTESIAN_POINT('Ctrl Pts',(-1.31031787011808,11.3984679038714,8.13572368865045));
#16888=CARTESIAN_POINT('Ctrl Pts',(-1.3103207794967,11.4198139026414,8.13699388375853));
#16889=CARTESIAN_POINT('Ctrl Pts',(-1.31758431089996,11.4622394981386,8.13953179812764));
#16890=CARTESIAN_POINT('Ctrl Pts',(-1.35907815796224,11.537672550237,8.14459256541487));
#16891=CARTESIAN_POINT('Ctrl Pts',(-1.45358116491496,11.5970739784784,8.15089377747445));
#16892=CARTESIAN_POINT('Ctrl Pts',(-1.58624854838693,11.5819949407127,8.15841484313965));
#16893=CARTESIAN_POINT('Ctrl Pts',(-1.65902671058246,11.5089632960888,8.16423427629322));
#16894=CARTESIAN_POINT('Ctrl Pts',(-1.68195987217319,11.4429652974819,8.16837694378074));
#16895=CARTESIAN_POINT('Ctrl Pts',(-1.688268126021,11.3875454584666,8.17168548379945));
#16896=CARTESIAN_POINT('Ctrl Pts',(-1.67247292588698,11.3184391587793,8.17581070456934));
#16897=CARTESIAN_POINT('Ctrl Pts',(-1.62399574898414,11.2577008228992,8.18033339280569));
#16898=CARTESIAN_POINT('Ctrl Pts',(-1.56298196453456,11.224038771947,8.18443316460721));
#16899=CARTESIAN_POINT('Ctrl Pts',(-1.50131080195971,11.2135623429727,8.18811404911797));
#16900=CARTESIAN_POINT('Ctrl Pts',(-1.43979480758285,11.2240327220399,8.19178613369517));
#16901=CARTESIAN_POINT('Ctrl Pts',(-1.38528198772036,11.2541593736133,8.1954495763896));
#16902=CARTESIAN_POINT('Ctrl Pts',(-1.34396297400778,11.3004801523066,8.19910449505273));
#16903=CARTESIAN_POINT('Ctrl Pts',(-1.31216358286281,11.3768384130203,8.20396661505384));
#16904=CARTESIAN_POINT('Ctrl Pts',(-1.32181429144628,11.4620867092022,8.20881209098619));
#16905=CARTESIAN_POINT('Ctrl Pts',(-1.36952635657431,11.5289357746158,8.21364196986567));
#16906=CARTESIAN_POINT('Ctrl Pts',(-1.43622482010054,11.5764654916456,8.21846152365081));
#16907=CARTESIAN_POINT('Ctrl Pts',(-1.54198775045592,11.5884277776652,8.22446681710422));
#16908=CARTESIAN_POINT('Ctrl Pts',(-1.64983940621575,11.5205830527132,8.23164417814806));
#16909=CARTESIAN_POINT('Ctrl Pts',(-1.69147661260008,11.4008602552993,8.23879406875351));
#16910=CARTESIAN_POINT('Ctrl Pts',(-1.64969906073525,11.2816165089832,8.24591762683419));
#16911=CARTESIAN_POINT('Ctrl Pts',(-1.54302760108597,11.2146949285323,8.25301643313596));
#16912=CARTESIAN_POINT('Ctrl Pts',(-1.41835572221323,11.2288076073328,8.26009205279526));
#16913=CARTESIAN_POINT('Ctrl Pts',(-1.32985553781733,11.317328148571,8.26714587979739));
#16914=CARTESIAN_POINT('Ctrl Pts',(-1.31609716199361,11.4412892120943,8.27417981680821));
#16915=CARTESIAN_POINT('Ctrl Pts',(-1.38232589747191,11.5466195616017,8.2811950801455));
#16916=CARTESIAN_POINT('Ctrl Pts',(-1.49950181041105,11.5875513852836,8.28819348662882));
#16917=CARTESIAN_POINT('Ctrl Pts',(-1.61642022374791,11.5467552025644,8.29517686219886));
#16918=CARTESIAN_POINT('Ctrl Pts',(-1.68213760009288,11.4419740685738,8.30214649665474));
#16919=CARTESIAN_POINT('Ctrl Pts',(-1.66830641134563,11.3193887587452,8.30910441881145));
#16920=CARTESIAN_POINT('Ctrl Pts',(-1.58110083006098,11.2321941107237,8.31605229547242));
#16921=CARTESIAN_POINT('Ctrl Pts',(-1.4792476035851,11.2208344821173,8.32183513940628));
#16922=CARTESIAN_POINT('Ctrl Pts',(-1.40667648021465,11.251073661914,8.32645839590582));
#16923=CARTESIAN_POINT('Ctrl Pts',(-1.3627496725696,11.2902560681181,8.32992431354831));
#16924=CARTESIAN_POINT('Ctrl Pts',(-1.33426997777496,11.3418492697892,8.33338935009938));
#16925=CARTESIAN_POINT('Ctrl Pts',(-1.32769859665103,11.3804625194559,8.33569768023126));
#16926=CARTESIAN_POINT('Ctrl Pts',(-1.32769594828092,11.399893457255,8.33685391951547));
#16927=CARTESIAN_POINT('Ctrl Pts',(-1.28760689691187,11.3984702171831,8.13573683219903));
#16928=CARTESIAN_POINT('Ctrl Pts',(-1.28761015030249,11.4223402188167,8.13715721826911));
#16929=CARTESIAN_POINT('Ctrl Pts',(-1.29574069823189,11.4698436668158,8.13999893186659));
#16930=CARTESIAN_POINT('Ctrl Pts',(-1.34220054404604,11.5543068887663,8.14566550688902));
#16931=CARTESIAN_POINT('Ctrl Pts',(-1.44804372097138,11.6208470149239,8.15272346527759));
#16932=CARTESIAN_POINT('Ctrl Pts',(-1.59667234436121,11.6039589503232,8.16114951450128));
#16933=CARTESIAN_POINT('Ctrl Pts',(-1.67820681832267,11.5221398896848,8.16766949698491));
#16934=CARTESIAN_POINT('Ctrl Pts',(-1.7038965373285,11.4482078712961,8.17231023317167));
#16935=CARTESIAN_POINT('Ctrl Pts',(-1.71096243409227,11.3861300306171,8.17601628495203));
#16936=CARTESIAN_POINT('Ctrl Pts',(-1.69327006673455,11.3087328100285,8.18063651015677));
#16937=CARTESIAN_POINT('Ctrl Pts',(-1.63898860213705,11.2407274405058,8.18570055349893));
#16938=CARTESIAN_POINT('Ctrl Pts',(-1.57069283693192,11.2030505087157,8.19028965641832));
#16939=CARTESIAN_POINT('Ctrl Pts',(-1.50168354422894,11.1913297753378,8.19440856412653));
#16940=CARTESIAN_POINT('Ctrl Pts',(-1.43287355273397,11.2030441435449,8.19851614600144));
#16941=CARTESIAN_POINT('Ctrl Pts',(-1.37192313191651,11.2367318400504,8.20261236550068));
#16942=CARTESIAN_POINT('Ctrl Pts',(-1.32574701623391,11.2885017430103,8.20669719317955));
#16943=CARTESIAN_POINT('Ctrl Pts',(-1.29022983260583,11.3737992937405,8.21212839868432));
#16944=CARTESIAN_POINT('Ctrl Pts',(-1.30101924761049,11.4689431694986,8.21753674265864));
#16945=CARTESIAN_POINT('Ctrl Pts',(-1.35422219641686,11.5434754519251,8.22292211134655));
#16946=CARTESIAN_POINT('Ctrl Pts',(-1.42854231555282,11.5964298939354,8.22829217190657));
#16947=CARTESIAN_POINT('Ctrl Pts',(-1.54625557984148,11.6097127216725,8.23497606414482));
#16948=CARTESIAN_POINT('Ctrl Pts',(-1.66606047372145,11.5342960575151,8.24295081727744));
#16949=CARTESIAN_POINT('Ctrl Pts',(-1.7121877671485,11.401518066656,8.2508797049335));
#16950=CARTESIAN_POINT('Ctrl Pts',(-1.66590689156277,11.269580018132,8.25876297847276));
#16951=CARTESIAN_POINT('Ctrl Pts',(-1.54810485222877,11.1957433036893,8.26660084978702));
#16952=CARTESIAN_POINT('Ctrl Pts',(-1.41080854120415,11.211346067515,8.27439362015181));
#16953=CARTESIAN_POINT('Ctrl Pts',(-1.31364913863162,11.3086211471592,8.28214172729599));
#16954=CARTESIAN_POINT('Ctrl Pts',(-1.29864878965667,11.4443899017918,8.2898455225234));
#16955=CARTESIAN_POINT('Ctrl Pts',(-1.37102274975831,11.5593586652546,8.29750567692185));
#16956=CARTESIAN_POINT('Ctrl Pts',(-1.49857402401843,11.6038349102434,8.30512273378781));
#16957=CARTESIAN_POINT('Ctrl Pts',(-1.62536272194757,11.559510894251,8.31269729907698));
#16958=CARTESIAN_POINT('Ctrl Pts',(-1.69631350739937,11.4462252895636,8.32023027155273));
#16959=CARTESIAN_POINT('Ctrl Pts',(-1.68133505571166,11.3142469851564,8.32772231203734));
#16960=CARTESIAN_POINT('Ctrl Pts',(-1.58774105874228,11.2207959961885,8.33517439949433));
#16961=CARTESIAN_POINT('Ctrl Pts',(-1.47893789023409,11.2087365622205,8.34135183809658));
#16962=CARTESIAN_POINT('Ctrl Pts',(-1.40167338285782,11.2409502757596,8.34627485215262));
#16963=CARTESIAN_POINT('Ctrl Pts',(-1.35500666141343,11.2825883188533,8.34995744593496));
#16964=CARTESIAN_POINT('Ctrl Pts',(-1.32482159324461,11.3372993457702,8.35363155056232));
#16965=CARTESIAN_POINT('Ctrl Pts',(-1.31787708279337,11.3781429992418,8.35607326612647));
#16966=CARTESIAN_POINT('Ctrl Pts',(-1.31787428424768,11.3986757665455,8.3572950698508));
#16967=CARTESIAN_POINT('Ctrl Pts',(-1.27206972759695,11.399625850708,8.11635166205074));
#16968=CARTESIAN_POINT('Ctrl Pts',(-1.272073217567,11.4252316265155,8.11787533548105));
#16969=CARTESIAN_POINT('Ctrl Pts',(-1.28079782866275,11.476240135189,8.12092681150558));
#16970=CARTESIAN_POINT('Ctrl Pts',(-1.33076456576505,11.5671179750832,8.12702348620128));
#16971=CARTESIAN_POINT('Ctrl Pts',(-1.44490392881093,11.638963378733,8.13463805879404));
#16972=CARTESIAN_POINT('Ctrl Pts',(-1.60582918091537,11.6207820721117,8.14376111980029));
#16973=CARTESIAN_POINT('Ctrl Pts',(-1.69446289809036,11.5319422031643,8.15084521913832));
#16974=CARTESIAN_POINT('Ctrl Pts',(-1.72244175741745,11.4514415195029,8.15589837968698));
#16975=CARTESIAN_POINT('Ctrl Pts',(-1.73014813242956,11.3837748524936,8.15993826176903));
#16976=CARTESIAN_POINT('Ctrl Pts',(-1.71085174681054,11.2992631614588,8.16498304728537));
#16977=CARTESIAN_POINT('Ctrl Pts',(-1.65147384017234,11.2248360286145,8.17052441820337));
#16978=CARTESIAN_POINT('Ctrl Pts',(-1.5766104517754,11.1835227037427,8.17555540643911));
#16979=CARTESIAN_POINT('Ctrl Pts',(-1.50084387946647,11.1706443178495,8.18007789437934));
#16980=CARTESIAN_POINT('Ctrl Pts',(-1.42517750444941,11.1835162317659,8.18459484543037));
#16981=CARTESIAN_POINT('Ctrl Pts',(-1.35805012154687,11.220606699589,8.18910601180499));
#16982=CARTESIAN_POINT('Ctrl Pts',(-1.30711690842411,11.277697611386,8.19361125027287));
#16983=CARTESIAN_POINT('Ctrl Pts',(-1.26787747114228,11.3718980721259,8.19960992779527));
#16984=CARTESIAN_POINT('Ctrl Pts',(-1.27977370153111,11.4772085311237,8.20559636673184));
#16985=CARTESIAN_POINT('Ctrl Pts',(-1.33876819889172,11.5598751165138,8.21156889433398));
#16986=CARTESIAN_POINT('Ctrl Pts',(-1.42128926663534,11.6186864604569,8.21753219718575));
#16987=CARTESIAN_POINT('Ctrl Pts',(-1.5522471277469,11.633518703715,8.22496891992462));
#16988=CARTESIAN_POINT('Ctrl Pts',(-1.68589445692796,11.549465051792,8.23386310316155));
#16989=CARTESIAN_POINT('Ctrl Pts',(-1.73750870098675,11.4010677271027,8.24272586927199));
#16990=CARTESIAN_POINT('Ctrl Pts',(-1.68572020536886,11.2532648112579,8.25155626087505));
#16991=CARTESIAN_POINT('Ctrl Pts',(-1.55353819609954,11.170356473708,8.26035285886125));
#16992=CARTESIAN_POINT('Ctrl Pts',(-1.39917195847527,11.187854450373,8.26911438227225));
#16993=CARTESIAN_POINT('Ctrl Pts',(-1.28973097737209,11.2973687066173,8.27783979028042));
#16994=CARTESIAN_POINT('Ctrl Pts',(-1.27277976962585,11.4504780098154,8.2865277145609));
#16995=CARTESIAN_POINT('Ctrl Pts',(-1.35447680269196,11.5803143436905,8.29517739991718));
#16996=CARTESIAN_POINT('Ctrl Pts',(-1.49865267270644,11.6306153145192,8.30378775302138));
#16997=CARTESIAN_POINT('Ctrl Pts',(-1.64211025739199,11.5804868435285,8.31235773520314));
#16998=CARTESIAN_POINT('Ctrl Pts',(-1.7224570532204,11.4522319009699,8.32088673450876));
#16999=CARTESIAN_POINT('Ctrl Pts',(-1.70550104906413,11.3027258546592,8.32937374827273));
#17000=CARTESIAN_POINT('Ctrl Pts',(-1.59944811600166,11.1968272197785,8.33781819530761));
#17001=CARTESIAN_POINT('Ctrl Pts',(-1.47614309313468,11.1831615633921,8.34481907931245));
#17002=CARTESIAN_POINT('Ctrl Pts',(-1.38858544995499,11.2196682102874,8.35039796002174));
#17003=CARTESIAN_POINT('Ctrl Pts',(-1.33570803330954,11.2668501746237,8.35457078800643));
#17004=CARTESIAN_POINT('Ctrl Pts',(-1.30151040777237,11.3288340399764,8.35873324545367));
#17005=CARTESIAN_POINT('Ctrl Pts',(-1.2936452922713,11.3751101882842,8.36149970184308));
#17006=CARTESIAN_POINT('Ctrl Pts',(-1.29364212612588,11.3983400134707,8.3628819941814));
#17007=CARTESIAN_POINT('Ctrl Pts',(-1.27763754668486,11.4010626531852,8.0921930248373));
#17008=CARTESIAN_POINT('Ctrl Pts',(-1.27764095442843,11.4260651364545,8.0936807993041));
#17009=CARTESIAN_POINT('Ctrl Pts',(-1.28615320916174,11.4758753899508,8.09666036655617));
#17010=CARTESIAN_POINT('Ctrl Pts',(-1.33504487783672,11.5648482537152,8.10262870832185));
#17011=CARTESIAN_POINT('Ctrl Pts',(-1.44708138024842,11.6354773294518,8.11010596916687));
#17012=CARTESIAN_POINT('Ctrl Pts',(-1.60582405260784,11.617666977309,8.1191045182285));
#17013=CARTESIAN_POINT('Ctrl Pts',(-1.69369436310896,11.5297138692624,8.1261221606495));
#17014=CARTESIAN_POINT('Ctrl Pts',(-1.72150184310992,11.4497283937332,8.13114290106676));
#17015=CARTESIAN_POINT('Ctrl Pts',(-1.72917491014276,11.3823989916055,8.13516273399635));
#17016=CARTESIAN_POINT('Ctrl Pts',(-1.7099594536617,11.2981149941292,8.14019350190391));
#17017=CARTESIAN_POINT('Ctrl Pts',(-1.65059645034948,11.2236567193758,8.14573566947207));
#17018=CARTESIAN_POINT('Ctrl Pts',(-1.57553615804699,11.1822164485617,8.15078027222728));
#17019=CARTESIAN_POINT('Ctrl Pts',(-1.4993988922352,11.1692607028417,8.15532498523488));
#17020=CARTESIAN_POINT('Ctrl Pts',(-1.42319050824966,11.1822104394915,8.15987410280572));
#17021=CARTESIAN_POINT('Ctrl Pts',(-1.35542885548834,11.2196341622936,8.16442737466481));
#17022=CARTESIAN_POINT('Ctrl Pts',(-1.30389697722355,11.2773765730482,8.16898463663304));
#17023=CARTESIAN_POINT('Ctrl Pts',(-1.26409872009562,11.3728617113105,8.1750658775057));
#17024=CARTESIAN_POINT('Ctrl Pts',(-1.27612377949662,11.4799801665083,8.1811546247418));
#17025=CARTESIAN_POINT('Ctrl Pts',(-1.33630832211724,11.5643498417057,8.18724907386285));
#17026=CARTESIAN_POINT('Ctrl Pts',(-1.42068242214268,11.6245048159568,8.19334733048934));
#17027=CARTESIAN_POINT('Ctrl Pts',(-1.55502413698417,11.639817184239,8.20097716406307));
#17028=CARTESIAN_POINT('Ctrl Pts',(-1.6927941330878,11.553313958365,8.21014169203597));
#17029=CARTESIAN_POINT('Ctrl Pts',(-1.74631350068157,11.3997899437419,8.21931277046328));
#17030=CARTESIAN_POINT('Ctrl Pts',(-1.69260588644463,11.2461610598641,8.22848927971837));
#17031=CARTESIAN_POINT('Ctrl Pts',(-1.55473056436024,11.1595461863356,8.2376691021646));
#17032=CARTESIAN_POINT('Ctrl Pts',(-1.3929635831252,11.1777694270612,8.2468502527565));
#17033=CARTESIAN_POINT('Ctrl Pts',(-1.27773348866187,11.2929146306548,8.2560312692688));
#17034=CARTESIAN_POINT('Ctrl Pts',(-1.25971626617438,11.4546519600478,8.26520946991855));
#17035=CARTESIAN_POINT('Ctrl Pts',(-1.34627233372441,11.5924167524738,8.27438404750244));
#17036=CARTESIAN_POINT('Ctrl Pts',(-1.49975074422118,11.6460771786317,8.28355270999763));
#17037=CARTESIAN_POINT('Ctrl Pts',(-1.65311797842412,11.5925962386231,8.29271320660328));
#17038=CARTESIAN_POINT('Ctrl Pts',(-1.73940864475926,11.455046521271,8.30186479981915));
#17039=CARTESIAN_POINT('Ctrl Pts',(-1.72124558283545,11.2940400614803,8.31100483551673));
#17040=CARTESIAN_POINT('Ctrl Pts',(-1.60669768511053,11.1795214471621,8.32013178525789));
#17041=CARTESIAN_POINT('Ctrl Pts',(-1.47297221979758,11.1646267451204,8.32772540801896));
#17042=CARTESIAN_POINT('Ctrl Pts',(-1.37776010024665,11.2043066055738,8.33379152241297));
#17043=CARTESIAN_POINT('Ctrl Pts',(-1.32016235023402,11.255689760052,8.33833673941345));
#17044=CARTESIAN_POINT('Ctrl Pts',(-1.28284406388789,11.3232978746022,8.34287743177524));
#17045=CARTESIAN_POINT('Ctrl Pts',(-1.27424115607837,11.3738832394125,8.34590176620214));
#17046=CARTESIAN_POINT('Ctrl Pts',(-1.27423769759512,11.3992579302876,8.34741168892013));
#17047=CARTESIAN_POINT('Ctrl Pts',(-1.29252021996078,11.4014860194052,8.08504414346851));
#17048=CARTESIAN_POINT('Ctrl Pts',(-1.29252340270791,11.4248377124435,8.08643368755038));
#17049=CARTESIAN_POINT('Ctrl Pts',(-1.30046778114425,11.4713320590255,8.08921465996777));
#17050=CARTESIAN_POINT('Ctrl Pts',(-1.34614564637204,11.5544752825906,8.09479162883554));
#17051=CARTESIAN_POINT('Ctrl Pts',(-1.45095047324357,11.6205843506291,8.10178650414618));
#17052=CARTESIAN_POINT('Ctrl Pts',(-1.59974527248719,11.6039399714675,8.11022032527475));
#17053=CARTESIAN_POINT('Ctrl Pts',(-1.68229004850136,11.5213719624091,8.11680945667679));
#17054=CARTESIAN_POINT('Ctrl Pts',(-1.70844117370727,11.4461617793564,8.12153032202421));
#17055=CARTESIAN_POINT('Ctrl Pts',(-1.71566331826827,11.3828110966603,8.12531255933759));
#17056=CARTESIAN_POINT('Ctrl Pts',(-1.69757750834476,11.3034240345936,8.13005070241393));
#17057=CARTESIAN_POINT('Ctrl Pts',(-1.64160013521397,11.2331886862249,8.13527755742201));
#17058=CARTESIAN_POINT('Ctrl Pts',(-1.57072270984747,11.1940485663383,8.14004092521617));
#17059=CARTESIAN_POINT('Ctrl Pts',(-1.49874863189192,11.181794166139,8.14433693625915));
#17060=CARTESIAN_POINT('Ctrl Pts',(-1.42662641616115,11.1940425084361,8.14864174461986));
#17061=CARTESIAN_POINT('Ctrl Pts',(-1.36242438483335,11.2294919242436,8.15295529955877));
#17062=CARTESIAN_POINT('Ctrl Pts',(-1.3135422927578,11.2842556577695,8.15727738161596));
#17063=CARTESIAN_POINT('Ctrl Pts',(-1.27574207341297,11.374919392659,8.16305164664494));
#17064=CARTESIAN_POINT('Ctrl Pts',(-1.28714343897904,11.4768148002382,8.16884166728008));
#17065=CARTESIAN_POINT('Ctrl Pts',(-1.3444869194707,11.5572200982027,8.17464880313036));
#17066=CARTESIAN_POINT('Ctrl Pts',(-1.42497778885075,11.6146185058939,8.18046654382713));
#17067=CARTESIAN_POINT('Ctrl Pts',(-1.55337347636932,11.6293057653988,8.18775734054507));
#17068=CARTESIAN_POINT('Ctrl Pts',(-1.68541834585444,11.5464796642254,8.19653638788628));
#17069=CARTESIAN_POINT('Ctrl Pts',(-1.73689409463485,11.3990227508843,8.20534519897164));
#17070=CARTESIAN_POINT('Ctrl Pts',(-1.68523728436395,11.251042071324,8.21418090745344));
#17071=CARTESIAN_POINT('Ctrl Pts',(-1.55214197761537,11.1673437610392,8.22304287959379));
#17072=CARTESIAN_POINT('Ctrl Pts',(-1.39551338149599,11.1849159837477,8.2319301178537));
#17073=CARTESIAN_POINT('Ctrl Pts',(-1.28359613434846,11.2966476765845,8.24084037449346));
#17074=CARTESIAN_POINT('Ctrl Pts',(-1.26598455202111,11.454093303528,8.24977423222552));
#17075=CARTESIAN_POINT('Ctrl Pts',(-1.35042026186512,11.5886190463113,8.25872779404424));
#17076=CARTESIAN_POINT('Ctrl Pts',(-1.50064630447962,11.6412209801601,8.26770068540722));
#17077=CARTESIAN_POINT('Ctrl Pts',(-1.65123772025323,11.5887907314702,8.27669243833904));
#17078=CARTESIAN_POINT('Ctrl Pts',(-1.73626813885955,11.4534107932928,8.28569896454702));
#17079=CARTESIAN_POINT('Ctrl Pts',(-1.71842046199703,11.2944302352445,8.29472073765604));
#17080=CARTESIAN_POINT('Ctrl Pts',(-1.60505722274475,11.1809734626463,8.30375561496672));
#17081=CARTESIAN_POINT('Ctrl Pts',(-1.47227067132104,11.1661175276503,8.31129378320585));
#17082=CARTESIAN_POINT('Ctrl Pts',(-1.37750166152921,11.2055980706118,8.31733044386806));
#17083=CARTESIAN_POINT('Ctrl Pts',(-1.3200893731747,11.256809238032,8.32186011665833));
#17084=CARTESIAN_POINT('Ctrl Pts',(-1.28283214929874,11.3242864598716,8.32639174504858));
#17085=CARTESIAN_POINT('Ctrl Pts',(-1.274229714894,11.3748629838859,8.3294148113833));
#17086=CARTESIAN_POINT('Ctrl Pts',(-1.27422625623265,11.4002389814767,8.33092481185749));
#17087=CARTESIAN_POINT('Ctrl Pts',(-1.30000020239985,11.401484999912,8.08504414346851));
#17088=CARTESIAN_POINT('Ctrl Pts',(-1.30000327196951,11.4240063142585,8.08638427580987));
#17089=CARTESIAN_POINT('Ctrl Pts',(-1.30766195210704,11.4688296121143,8.08906540106247));
#17090=CARTESIAN_POINT('Ctrl Pts',(-1.35170527056063,11.5490007767019,8.09444309083296));
#17091=CARTESIAN_POINT('Ctrl Pts',(-1.45277519214087,11.6127580060184,8.10118931860474));
#17092=CARTESIAN_POINT('Ctrl Pts',(-1.59631200820559,11.5967080298454,8.10932541726778));
#17093=CARTESIAN_POINT('Ctrl Pts',(-1.67596957869062,11.5170338262931,8.11568426491253));
#17094=CARTESIAN_POINT('Ctrl Pts',(-1.70121188840275,11.4444384060934,8.1202410535319));
#17095=CARTESIAN_POINT('Ctrl Pts',(-1.70818405294183,11.3832823318955,8.12389232718534));
#17096=CARTESIAN_POINT('Ctrl Pts',(-1.69072329377588,11.3066287277546,8.12846738314285));
#17097=CARTESIAN_POINT('Ctrl Pts',(-1.63665950516375,11.238790127298,8.13351592412261));
#17098=CARTESIAN_POINT('Ctrl Pts',(-1.56818361973235,11.2009745480362,8.13811814384478));
#17099=CARTESIAN_POINT('Ctrl Pts',(-1.49863040169783,11.1891308835848,8.14226983820643));
#17100=CARTESIAN_POINT('Ctrl Pts',(-1.42891504240342,11.200968879272,8.14643117635655));
#17101=CARTESIAN_POINT('Ctrl Pts',(-1.3668378439393,11.2352429623094,8.1506021000395));
#17102=CARTESIAN_POINT('Ctrl Pts',(-1.31955925093111,11.28820773555,8.15478254820105));
#17103=CARTESIAN_POINT('Ctrl Pts',(-1.2829867844608,11.3759192191191,8.16036908991613));
#17104=CARTESIAN_POINT('Ctrl Pts',(-1.29401152106405,11.4745465130164,8.16597441543018));
#17105=CARTESIAN_POINT('Ctrl Pts',(-1.34954004839579,11.552412334257,8.17159821912675));
#17106=CARTESIAN_POINT('Ctrl Pts',(-1.42751096236488,11.6080171412814,8.17723423461392));
#17107=CARTESIAN_POINT('Ctrl Pts',(-1.55195451138358,11.6222672514631,8.18430195037065));
#17108=CARTESIAN_POINT('Ctrl Pts',(-1.68004289685552,11.5419454250746,8.19281879836256));
#17109=CARTESIAN_POINT('Ctrl Pts',(-1.73003116645036,11.3988109655711,8.20137045479898));
#17110=CARTESIAN_POINT('Ctrl Pts',(-1.67986342570098,11.2550353636857,8.20995610504997));
#17111=CARTESIAN_POINT('Ctrl Pts',(-1.55045492335515,11.1736299517761,8.21857485832766));
#17112=CARTESIAN_POINT('Ctrl Pts',(-1.39801143573852,11.1907087568511,8.22722577082007));
#17113=CARTESIAN_POINT('Ctrl Pts',(-1.28896559860806,11.2995363829214,8.23590787035433));
#17114=CARTESIAN_POINT('Ctrl Pts',(-1.27176576818906,11.4530596594369,8.2446200855233));
#17115=CARTESIAN_POINT('Ctrl Pts',(-1.35415676648766,11.5843816465237,8.25336136935291));
#17116=CARTESIAN_POINT('Ctrl Pts',(-1.50092826267245,11.6358042592741,8.26213056504353));
#17117=CARTESIAN_POINT('Ctrl Pts',(-1.64822931811663,11.5845480275544,8.27092648209213));
#17118=CARTESIAN_POINT('Ctrl Pts',(-1.73150905278482,11.452001965896,8.27974794260049));
#17119=CARTESIAN_POINT('Ctrl Pts',(-1.71403680175737,11.2961559302974,8.28859365842336));
#17120=CARTESIAN_POINT('Ctrl Pts',(-1.60280104690191,11.1847900297702,8.2974622924596));
#17121=CARTESIAN_POINT('Ctrl Pts',(-1.47233026209572,11.1701693264817,8.30487091671699));
#17122=CARTESIAN_POINT('Ctrl Pts',(-1.37913177644534,11.2089883543221,8.31080779458597));
#17123=CARTESIAN_POINT('Ctrl Pts',(-1.32263542974685,11.2593763422036,8.31526551319425));
#17124=CARTESIAN_POINT('Ctrl Pts',(-1.28594863227905,11.3258070419811,8.31972744443214));
#17125=CARTESIAN_POINT('Ctrl Pts',(-1.27746839178067,11.3756346212766,8.3227063400453));
#17126=CARTESIAN_POINT('Ctrl Pts',(-1.27746498364382,11.4006399235282,8.32419428226795));
#17127=CARTESIAN_POINT('',(-1.30000020239985,11.401484999912,8.08504414346851));
#17128=CARTESIAN_POINT('Origin',(-1.3,11.4,8.11));
#17129=CARTESIAN_POINT('',(-1.27746498364382,11.4006399235282,8.32419428226795));
#17130=CARTESIAN_POINT('Ctrl Pts',(-1.30000020239985,11.401484999912,8.08504414346851));
#17131=CARTESIAN_POINT('Ctrl Pts',(-1.30000327196951,11.4240063142585,8.08638427580987));
#17132=CARTESIAN_POINT('Ctrl Pts',(-1.30766195210704,11.4688296121143,8.08906540106247));
#17133=CARTESIAN_POINT('Ctrl Pts',(-1.35170527056063,11.5490007767019,8.09444309083296));
#17134=CARTESIAN_POINT('Ctrl Pts',(-1.45277519214087,11.6127580060184,8.10118931860474));
#17135=CARTESIAN_POINT('Ctrl Pts',(-1.59631200820559,11.5967080298454,8.10932541726778));
#17136=CARTESIAN_POINT('Ctrl Pts',(-1.67596957869062,11.5170338262931,8.11568426491253));
#17137=CARTESIAN_POINT('Ctrl Pts',(-1.70121188840275,11.4444384060934,8.1202410535319));
#17138=CARTESIAN_POINT('Ctrl Pts',(-1.70818405294183,11.3832823318955,8.12389232718534));
#17139=CARTESIAN_POINT('Ctrl Pts',(-1.69072329377588,11.3066287277546,8.12846738314285));
#17140=CARTESIAN_POINT('Ctrl Pts',(-1.63665950516375,11.238790127298,8.13351592412261));
#17141=CARTESIAN_POINT('Ctrl Pts',(-1.56818361973235,11.2009745480362,8.13811814384478));
#17142=CARTESIAN_POINT('Ctrl Pts',(-1.49863040169783,11.1891308835848,8.14226983820643));
#17143=CARTESIAN_POINT('Ctrl Pts',(-1.42891504240342,11.200968879272,8.14643117635655));
#17144=CARTESIAN_POINT('Ctrl Pts',(-1.3668378439393,11.2352429623094,8.1506021000395));
#17145=CARTESIAN_POINT('Ctrl Pts',(-1.31955925093111,11.28820773555,8.15478254820105));
#17146=CARTESIAN_POINT('Ctrl Pts',(-1.2829867844608,11.3759192191191,8.16036908991613));
#17147=CARTESIAN_POINT('Ctrl Pts',(-1.29401152106405,11.4745465130164,8.16597441543018));
#17148=CARTESIAN_POINT('Ctrl Pts',(-1.34954004839579,11.552412334257,8.17159821912675));
#17149=CARTESIAN_POINT('Ctrl Pts',(-1.42751096236488,11.6080171412814,8.17723423461392));
#17150=CARTESIAN_POINT('Ctrl Pts',(-1.55195451138358,11.6222672514631,8.18430195037065));
#17151=CARTESIAN_POINT('Ctrl Pts',(-1.68004289685552,11.5419454250746,8.19281879836256));
#17152=CARTESIAN_POINT('Ctrl Pts',(-1.73003116645036,11.3988109655711,8.20137045479898));
#17153=CARTESIAN_POINT('Ctrl Pts',(-1.67986342570098,11.2550353636857,8.20995610504997));
#17154=CARTESIAN_POINT('Ctrl Pts',(-1.55045492335515,11.1736299517761,8.21857485832766));
#17155=CARTESIAN_POINT('Ctrl Pts',(-1.39801143573852,11.1907087568511,8.22722577082007));
#17156=CARTESIAN_POINT('Ctrl Pts',(-1.28896559860806,11.2995363829214,8.23590787035433));
#17157=CARTESIAN_POINT('Ctrl Pts',(-1.27176576818906,11.4530596594369,8.2446200855233));
#17158=CARTESIAN_POINT('Ctrl Pts',(-1.35415676648766,11.5843816465237,8.25336136935291));
#17159=CARTESIAN_POINT('Ctrl Pts',(-1.50092826267245,11.6358042592741,8.26213056504353));
#17160=CARTESIAN_POINT('Ctrl Pts',(-1.64822931811663,11.5845480275544,8.27092648209213));
#17161=CARTESIAN_POINT('Ctrl Pts',(-1.73150905278482,11.452001965896,8.27974794260049));
#17162=CARTESIAN_POINT('Ctrl Pts',(-1.71403680175737,11.2961559302974,8.28859365842336));
#17163=CARTESIAN_POINT('Ctrl Pts',(-1.60280104690191,11.1847900297702,8.2974622924596));
#17164=CARTESIAN_POINT('Ctrl Pts',(-1.47233026209572,11.1701693264817,8.30487091671699));
#17165=CARTESIAN_POINT('Ctrl Pts',(-1.37913177644534,11.2089883543221,8.31080779458597));
#17166=CARTESIAN_POINT('Ctrl Pts',(-1.32263542974685,11.2593763422036,8.31526551319425));
#17167=CARTESIAN_POINT('Ctrl Pts',(-1.28594863227905,11.3258070419811,8.31972744443214));
#17168=CARTESIAN_POINT('Ctrl Pts',(-1.27746839178067,11.3756346212766,8.3227063400453));
#17169=CARTESIAN_POINT('Ctrl Pts',(-1.27746498364382,11.4006399235282,8.32419428226795));
#17170=CARTESIAN_POINT('Origin',(-1.3,11.4,8.335));
#17171=CARTESIAN_POINT('Origin',(-1.3,11.4,8.335));
#17172=CARTESIAN_POINT('Origin',(-1.3,11.4,8.11));
#18936=UNCERTAINTY_MEASURE_WITH_UNIT(LENGTH_MEASURE(0.001),#19044,
'DISTANCE_ACCURACY_VALUE',
'Maximum model space distance between geometric entities at asserted c
onnectivities');
#18972=UNCERTAINTY_MEASURE_WITH_UNIT(LENGTH_MEASURE(0.001),#19044,
'DISTANCE_ACCURACY_VALUE',
'Maximum model space distance between geometric entities at asserted c
onnectivities');
#19007=(
GEOMETRIC_REPRESENTATION_CONTEXT(3)
GLOBAL_UNCERTAINTY_ASSIGNED_CONTEXT((#18936))
GLOBAL_UNIT_ASSIGNED_CONTEXT((#19044,#19046,#19047))
REPRESENTATION_CONTEXT('','3D')
);
#19043=(
GEOMETRIC_REPRESENTATION_CONTEXT(3)
GLOBAL_UNCERTAINTY_ASSIGNED_CONTEXT((#18972))
GLOBAL_UNIT_ASSIGNED_CONTEXT((#19044,#19046,#19047))
REPRESENTATION_CONTEXT('','3D')
);
#19044=(
LENGTH_UNIT()
NAMED_UNIT(*)
SI_UNIT(.CENTI.,.METRE.)
);
#19046=(
NAMED_UNIT(*)
PLANE_ANGLE_UNIT()
SI_UNIT($,.RADIAN.)
);
#19047=(
NAMED_UNIT(*)
SI_UNIT($,.STERADIAN.)
SOLID_ANGLE_UNIT()
);
#19082=SHAPE_DEFINITION_REPRESENTATION(#19157,#19340);
#19157=PRODUCT_DEFINITION_SHAPE('',$,#19411);
#19340=SHAPE_REPRESENTATION('',(#10954),#19007);
#19376=PRODUCT_DEFINITION_CONTEXT('part definition',#19588,'design');
#19411=PRODUCT_DEFINITION('2026-11-03-00-38-46-490',
'Inlet return spring',#19481,#19376);
#19481=PRODUCT_DEFINITION_FORMATION('',$,#19624);
#19588=APPLICATION_CONTEXT(
'Core Data for Automotive Mechanical Design Process');
#19589=PRODUCT_CONTEXT('part definition',#19588,'mechanical');
#19624=PRODUCT('2026-11-03-00-38-46-490','Inlet return spring',
'Inlet return spring',(#19589));
#19664=PRESENTATION_STYLE_ASSIGNMENT((#19670));
#19670=SURFACE_STYLE_USAGE(.BOTH.,#19676);
#19676=SURFACE_SIDE_STYLE('',(#19682));
#19682=SURFACE_STYLE_FILL_AREA(#19688);
#19688=FILL_AREA_STYLE('CAD Library Painted - Steel gray',(#19694));
#19694=FILL_AREA_STYLE_COLOUR('CAD Library Painted - Steel gray',#19700);
#19700=COLOUR_RGB('CAD Library Painted - Steel gray',0.592156862745098,
0.631372549019608,0.67843137254902);
ENDSEC;
END-ISO-10303-21;
